ISO-10303-21;
HEADER;
/* Generated by software containing ST-Developer
 * from STEP Tools, Inc. (www.steptools.com) 
 */

FILE_DESCRIPTION(
/* description */ ('Manual piston pump'),
/* implementation_level */ '2;1');

FILE_NAME(
/* name */ 'M5x30 frame screw.step',
/* time_stamp */ '2026-11-02T16:54:23-08:00',
/* author */ (''),
/* organization */ (''),
/* preprocessor_version */ 'ST-DEVELOPER v20.2',
/* originating_system */ 'Autodesk Translation Framework v15.17.0.0',
/* authorisation */ '');

FILE_SCHEMA (('AUTOMOTIVE_DESIGN { 1 0 10303 214 3 1 1 }'));
ENDSEC;

DATA;
#10=MECHANICAL_DESIGN_GEOMETRIC_PRESENTATION_REPRESENTATION('',(#709),#19043);
#523=ORIENTED_CLOSED_SHELL('',*,#9494,.F.);
#534=CONICAL_SURFACE('',#10657,0.4,0.785398163397448);
#535=CONICAL_SURFACE('',#10661,0.41,0.785398163397448);
#536=CONICAL_SURFACE('',#10665,0.26,0.463647609000806);
#554=BREP_WITH_VOIDS('Body1',#9495,(#523));
#583=SHAPE_REPRESENTATION_RELATIONSHIP('SRR','None',#19329,#646);
#646=ADVANCED_BREP_SHAPE_REPRESENTATION('',(#554),#18996);
#709=STYLED_ITEM('',(#19663),#554);
#928=FACE_BOUND('',#2180,.T.);
#929=FACE_BOUND('',#2188,.T.);
#1171=CYLINDRICAL_SURFACE('',#10652,0.25);
#1172=CYLINDRICAL_SURFACE('',#10659,0.425);
#1173=CYLINDRICAL_SURFACE('',#10667,0.24505);
#1495=FACE_OUTER_BOUND('',#2171,.T.);
#1496=FACE_OUTER_BOUND('',#2172,.T.);
#1497=FACE_OUTER_BOUND('',#2173,.T.);
#1498=FACE_OUTER_BOUND('',#2174,.T.);
#1499=FACE_OUTER_BOUND('',#2175,.T.);
#1500=FACE_OUTER_BOUND('',#2176,.T.);
#1501=FACE_OUTER_BOUND('',#2177,.T.);
#1502=FACE_OUTER_BOUND('',#2178,.T.);
#1503=FACE_OUTER_BOUND('',#2179,.T.);
#1504=FACE_OUTER_BOUND('',#2181,.T.);
#1505=FACE_OUTER_BOUND('',#2182,.T.);
#1506=FACE_OUTER_BOUND('',#2183,.T.);
#1507=FACE_OUTER_BOUND('',#2184,.T.);
#1508=FACE_OUTER_BOUND('',#2185,.T.);
#1509=FACE_OUTER_BOUND('',#2186,.T.);
#1510=FACE_OUTER_BOUND('',#2187,.T.);
#1511=FACE_OUTER_BOUND('',#2189,.T.);
#1512=FACE_OUTER_BOUND('',#2190,.T.);
#2171=EDGE_LOOP('',(#7105,#7106,#7107,#7108));
#2172=EDGE_LOOP('',(#7109,#7110,#7111,#7112));
#2173=EDGE_LOOP('',(#7113,#7114,#7115,#7116));
#2174=EDGE_LOOP('',(#7117,#7118,#7119,#7120));
#2175=EDGE_LOOP('',(#7121,#7122,#7123,#7124));
#2176=EDGE_LOOP('',(#7125,#7126,#7127,#7128));
#2177=EDGE_LOOP('',(#7129,#7130,#7131,#7132,#7133,#7134));
#2178=EDGE_LOOP('',(#7135,#7136,#7137,#7138,#7139,#7140));
#2179=EDGE_LOOP('',(#7141));
#2180=EDGE_LOOP('',(#7142));
#2181=EDGE_LOOP('',(#7143,#7144,#7145,#7146));
#2182=EDGE_LOOP('',(#7147));
#2183=EDGE_LOOP('',(#7148));
#2184=EDGE_LOOP('',(#7149,#7150,#7151,#7152));
#2185=EDGE_LOOP('',(#7153,#7154,#7155,#7156));
#2186=EDGE_LOOP('',(#7157,#7158,#7159,#7160));
#2187=EDGE_LOOP('',(#7161));
#2188=EDGE_LOOP('',(#7162));
#2189=EDGE_LOOP('',(#7163,#7164,#7165,#7166));
#2190=EDGE_LOOP('',(#7167,#7168,#7169,#7170));
#2834=CIRCLE('',#10650,0.25);
#2835=CIRCLE('',#10651,0.24505);
#2836=CIRCLE('',#10653,0.25);
#2837=CIRCLE('',#10656,0.375);
#2838=CIRCLE('',#10658,0.425);
#2839=CIRCLE('',#10660,0.425);
#2840=CIRCLE('',#10662,0.395);
#2841=CIRCLE('',#10664,0.27);
#2842=CIRCLE('',#10666,0.24505);
#3377=LINE('',#15598,#3981);
#3378=LINE('',#15600,#3982);
#3379=LINE('',#15602,#3983);
#3380=LINE('',#15603,#3984);
#3381=LINE('',#15606,#3985);
#3382=LINE('',#15608,#3986);
#3383=LINE('',#15609,#3987);
#3384=LINE('',#15612,#3988);
#3385=LINE('',#15614,#3989);
#3386=LINE('',#15615,#3990);
#3387=LINE('',#15618,#3991);
#3388=LINE('',#15620,#3992);
#3389=LINE('',#15621,#3993);
#3390=LINE('',#15624,#3994);
#3391=LINE('',#15626,#3995);
#3392=LINE('',#15627,#3996);
#3393=LINE('',#15629,#3997);
#3394=LINE('',#15630,#3998);
#3395=LINE('',#15640,#3999);
#3396=LINE('',#15649,#4000);
#3397=LINE('',#15653,#4001);
#3398=LINE('',#15657,#4002);
#3399=LINE('',#15664,#4003);
#3400=LINE('',#15666,#4004);
#3981=VECTOR('',#12523,1.);
#3982=VECTOR('',#12524,1.);
#3983=VECTOR('',#12525,1.);
#3984=VECTOR('',#12526,1.);
#3985=VECTOR('',#12529,1.);
#3986=VECTOR('',#12530,1.);
#3987=VECTOR('',#12531,1.);
#3988=VECTOR('',#12534,1.);
#3989=VECTOR('',#12535,1.);
#3990=VECTOR('',#12536,1.);
#3991=VECTOR('',#12539,1.);
#3992=VECTOR('',#12540,1.);
#3993=VECTOR('',#12541,1.);
#3994=VECTOR('',#12544,1.);
#3995=VECTOR('',#12545,1.);
#3996=VECTOR('',#12546,1.);
#3997=VECTOR('',#12549,1.);
#3998=VECTOR('',#12550,1.);
#3999=VECTOR('',#12563,0.25);
#4000=VECTOR('',#12576,0.4);
#4001=VECTOR('',#12581,0.425);
#4002=VECTOR('',#12586,0.41);
#4003=VECTOR('',#12595,0.26);
#4004=VECTOR('',#12598,0.25);
#4629=VERTEX_POINT('',#15596);
#4630=VERTEX_POINT('',#15597);
#4631=VERTEX_POINT('',#15599);
#4632=VERTEX_POINT('',#15601);
#4633=VERTEX_POINT('',#15605);
#4634=VERTEX_POINT('',#15607);
#4635=VERTEX_POINT('',#15611);
#4636=VERTEX_POINT('',#15613);
#4637=VERTEX_POINT('',#15617);
#4638=VERTEX_POINT('',#15619);
#4639=VERTEX_POINT('',#15623);
#4640=VERTEX_POINT('',#15625);
#4641=VERTEX_POINT('',#15634);
#4642=VERTEX_POINT('',#15636);
#4643=VERTEX_POINT('',#15639);
#4644=VERTEX_POINT('',#15644);
#4645=VERTEX_POINT('',#15647);
#4646=VERTEX_POINT('',#15651);
#4647=VERTEX_POINT('',#15655);
#4648=VERTEX_POINT('',#15659);
#4649=VERTEX_POINT('',#15662);
#5539=EDGE_CURVE('',#4629,#4630,#3377,.T.);
#5540=EDGE_CURVE('',#4630,#4631,#3378,.T.);
#5541=EDGE_CURVE('',#4631,#4632,#3379,.T.);
#5542=EDGE_CURVE('',#4629,#4632,#3380,.T.);
#5543=EDGE_CURVE('',#4630,#4633,#3381,.T.);
#5544=EDGE_CURVE('',#4633,#4634,#3382,.T.);
#5545=EDGE_CURVE('',#4634,#4631,#3383,.T.);
#5546=EDGE_CURVE('',#4633,#4635,#3384,.T.);
#5547=EDGE_CURVE('',#4635,#4636,#3385,.T.);
#5548=EDGE_CURVE('',#4636,#4634,#3386,.T.);
#5549=EDGE_CURVE('',#4635,#4637,#3387,.T.);
#5550=EDGE_CURVE('',#4637,#4638,#3388,.T.);
#5551=EDGE_CURVE('',#4638,#4636,#3389,.T.);
#5552=EDGE_CURVE('',#4637,#4639,#3390,.T.);
#5553=EDGE_CURVE('',#4639,#4640,#3391,.T.);
#5554=EDGE_CURVE('',#4640,#4638,#3392,.T.);
#5555=EDGE_CURVE('',#4639,#4629,#3393,.T.);
#5556=EDGE_CURVE('',#4632,#4640,#3394,.T.);
#5557=EDGE_CURVE('',#4641,#4641,#2834,.T.);
#5558=EDGE_CURVE('',#4642,#4642,#2835,.T.);
#5559=EDGE_CURVE('',#4641,#4643,#3395,.T.);
#5560=EDGE_CURVE('',#4643,#4643,#2836,.T.);
#5561=EDGE_CURVE('',#4644,#4644,#2837,.T.);
#5562=EDGE_CURVE('',#4645,#4645,#2838,.T.);
#5563=EDGE_CURVE('',#4645,#4644,#3396,.T.);
#5564=EDGE_CURVE('',#4646,#4646,#2839,.T.);
#5565=EDGE_CURVE('',#4646,#4645,#3397,.T.);
#5566=EDGE_CURVE('',#4647,#4647,#2840,.T.);
#5567=EDGE_CURVE('',#4647,#4646,#3398,.T.);
#5568=EDGE_CURVE('',#4648,#4648,#2841,.T.);
#5569=EDGE_CURVE('',#4649,#4649,#2842,.F.);
#5570=EDGE_CURVE('',#4649,#4648,#3399,.T.);
#5571=EDGE_CURVE('',#4642,#4649,#3400,.T.);
#7105=ORIENTED_EDGE('',*,*,#5539,.T.);
#7106=ORIENTED_EDGE('',*,*,#5540,.T.);
#7107=ORIENTED_EDGE('',*,*,#5541,.T.);
#7108=ORIENTED_EDGE('',*,*,#5542,.F.);
#7109=ORIENTED_EDGE('',*,*,#5543,.T.);
#7110=ORIENTED_EDGE('',*,*,#5544,.T.);
#7111=ORIENTED_EDGE('',*,*,#5545,.T.);
#7112=ORIENTED_EDGE('',*,*,#5540,.F.);
#7113=ORIENTED_EDGE('',*,*,#5546,.T.);
#7114=ORIENTED_EDGE('',*,*,#5547,.T.);
#7115=ORIENTED_EDGE('',*,*,#5548,.T.);
#7116=ORIENTED_EDGE('',*,*,#5544,.F.);
#7117=ORIENTED_EDGE('',*,*,#5549,.T.);
#7118=ORIENTED_EDGE('',*,*,#5550,.T.);
#7119=ORIENTED_EDGE('',*,*,#5551,.T.);
#7120=ORIENTED_EDGE('',*,*,#5547,.F.);
#7121=ORIENTED_EDGE('',*,*,#5552,.T.);
#7122=ORIENTED_EDGE('',*,*,#5553,.T.);
#7123=ORIENTED_EDGE('',*,*,#5554,.T.);
#7124=ORIENTED_EDGE('',*,*,#5550,.F.);
#7125=ORIENTED_EDGE('',*,*,#5555,.T.);
#7126=ORIENTED_EDGE('',*,*,#5542,.T.);
#7127=ORIENTED_EDGE('',*,*,#5556,.T.);
#7128=ORIENTED_EDGE('',*,*,#5553,.F.);
#7129=ORIENTED_EDGE('',*,*,#5555,.F.);
#7130=ORIENTED_EDGE('',*,*,#5552,.F.);
#7131=ORIENTED_EDGE('',*,*,#5549,.F.);
#7132=ORIENTED_EDGE('',*,*,#5546,.F.);
#7133=ORIENTED_EDGE('',*,*,#5543,.F.);
#7134=ORIENTED_EDGE('',*,*,#5539,.F.);
#7135=ORIENTED_EDGE('',*,*,#5556,.F.);
#7136=ORIENTED_EDGE('',*,*,#5541,.F.);
#7137=ORIENTED_EDGE('',*,*,#5545,.F.);
#7138=ORIENTED_EDGE('',*,*,#5548,.F.);
#7139=ORIENTED_EDGE('',*,*,#5551,.F.);
#7140=ORIENTED_EDGE('',*,*,#5554,.F.);
#7141=ORIENTED_EDGE('',*,*,#5557,.T.);
#7142=ORIENTED_EDGE('',*,*,#5558,.F.);
#7143=ORIENTED_EDGE('',*,*,#5557,.F.);
#7144=ORIENTED_EDGE('',*,*,#5559,.T.);
#7145=ORIENTED_EDGE('',*,*,#5560,.T.);
#7146=ORIENTED_EDGE('',*,*,#5559,.F.);
#7147=ORIENTED_EDGE('',*,*,#5560,.F.);
#7148=ORIENTED_EDGE('',*,*,#5561,.F.);
#7149=ORIENTED_EDGE('',*,*,#5562,.F.);
#7150=ORIENTED_EDGE('',*,*,#5563,.T.);
#7151=ORIENTED_EDGE('',*,*,#5561,.T.);
#7152=ORIENTED_EDGE('',*,*,#5563,.F.);
#7153=ORIENTED_EDGE('',*,*,#5564,.F.);
#7154=ORIENTED_EDGE('',*,*,#5565,.T.);
#7155=ORIENTED_EDGE('',*,*,#5562,.T.);
#7156=ORIENTED_EDGE('',*,*,#5565,.F.);
#7157=ORIENTED_EDGE('',*,*,#5566,.F.);
#7158=ORIENTED_EDGE('',*,*,#5567,.T.);
#7159=ORIENTED_EDGE('',*,*,#5564,.T.);
#7160=ORIENTED_EDGE('',*,*,#5567,.F.);
#7161=ORIENTED_EDGE('',*,*,#5566,.T.);
#7162=ORIENTED_EDGE('',*,*,#5568,.F.);
#7163=ORIENTED_EDGE('',*,*,#5569,.F.);
#7164=ORIENTED_EDGE('',*,*,#5570,.T.);
#7165=ORIENTED_EDGE('',*,*,#5568,.T.);
#7166=ORIENTED_EDGE('',*,*,#5570,.F.);
#7167=ORIENTED_EDGE('',*,*,#5558,.T.);
#7168=ORIENTED_EDGE('',*,*,#5571,.T.);
#7169=ORIENTED_EDGE('',*,*,#5569,.T.);
#7170=ORIENTED_EDGE('',*,*,#5571,.F.);
#8688=PLANE('',#10641);
#8689=PLANE('',#10642);
#8690=PLANE('',#10643);
#8691=PLANE('',#10644);
#8692=PLANE('',#10645);
#8693=PLANE('',#10646);
#8694=PLANE('',#10647);
#8695=PLANE('',#10648);
#8696=PLANE('',#10649);
#8697=PLANE('',#10654);
#8698=PLANE('',#10655);
#8699=PLANE('',#10663);
#9100=ADVANCED_FACE('',(#1495),#8688,.F.);
#9101=ADVANCED_FACE('',(#1496),#8689,.F.);
#9102=ADVANCED_FACE('',(#1497),#8690,.F.);
#9103=ADVANCED_FACE('',(#1498),#8691,.F.);
#9104=ADVANCED_FACE('',(#1499),#8692,.F.);
#9105=ADVANCED_FACE('',(#1500),#8693,.F.);
#9106=ADVANCED_FACE('',(#1501),#8694,.F.);
#9107=ADVANCED_FACE('',(#1502),#8695,.F.);
#9108=ADVANCED_FACE('',(#1503,#928),#8696,.T.);
#9109=ADVANCED_FACE('',(#1504),#1171,.T.);
#9110=ADVANCED_FACE('',(#1505),#8697,.F.);
#9111=ADVANCED_FACE('',(#1506),#8698,.T.);
#9112=ADVANCED_FACE('',(#1507),#534,.T.);
#9113=ADVANCED_FACE('',(#1508),#1172,.T.);
#9114=ADVANCED_FACE('',(#1509),#535,.T.);
#9115=ADVANCED_FACE('',(#1510,#929),#8699,.T.);
#9116=ADVANCED_FACE('',(#1511),#536,.T.);
#9117=ADVANCED_FACE('',(#1512),#1173,.T.);
#9494=CLOSED_SHELL('',(#9100,#9101,#9102,#9103,#9104,#9105,#9106,#9107));
#9495=CLOSED_SHELL('',(#9108,#9109,#9110,#9111,#9112,#9113,#9114,#9115,
#9116,#9117));
#10640=AXIS2_PLACEMENT_3D('',#15594,#12519,#12520);
#10641=AXIS2_PLACEMENT_3D('',#15595,#12521,#12522);
#10642=AXIS2_PLACEMENT_3D('',#15604,#12527,#12528);
#10643=AXIS2_PLACEMENT_3D('',#15610,#12532,#12533);
#10644=AXIS2_PLACEMENT_3D('',#15616,#12537,#12538);
#10645=AXIS2_PLACEMENT_3D('',#15622,#12542,#12543);
#10646=AXIS2_PLACEMENT_3D('',#15628,#12547,#12548);
#10647=AXIS2_PLACEMENT_3D('',#15631,#12551,#12552);
#10648=AXIS2_PLACEMENT_3D('',#15632,#12553,#12554);
#10649=AXIS2_PLACEMENT_3D('',#15633,#12555,#12556);
#10650=AXIS2_PLACEMENT_3D('',#15635,#12557,#12558);
#10651=AXIS2_PLACEMENT_3D('',#15637,#12559,#12560);
#10652=AXIS2_PLACEMENT_3D('',#15638,#12561,#12562);
#10653=AXIS2_PLACEMENT_3D('',#15641,#12564,#12565);
#10654=AXIS2_PLACEMENT_3D('',#15642,#12566,#12567);
#10655=AXIS2_PLACEMENT_3D('',#15643,#12568,#12569);
#10656=AXIS2_PLACEMENT_3D('',#15645,#12570,#12571);
#10657=AXIS2_PLACEMENT_3D('',#15646,#12572,#12573);
#10658=AXIS2_PLACEMENT_3D('',#15648,#12574,#12575);
#10659=AXIS2_PLACEMENT_3D('',#15650,#12577,#12578);
#10660=AXIS2_PLACEMENT_3D('',#15652,#12579,#12580);
#10661=AXIS2_PLACEMENT_3D('',#15654,#12582,#12583);
#10662=AXIS2_PLACEMENT_3D('',#15656,#12584,#12585);
#10663=AXIS2_PLACEMENT_3D('',#15658,#12587,#12588);
#10664=AXIS2_PLACEMENT_3D('',#15660,#12589,#12590);
#10665=AXIS2_PLACEMENT_3D('',#15661,#12591,#12592);
#10666=AXIS2_PLACEMENT_3D('',#15663,#12593,#12594);
#10667=AXIS2_PLACEMENT_3D('',#15665,#12596,#12597);
#12519=DIRECTION('axis',(0.,0.,1.));
#12520=DIRECTION('refdir',(1.,0.,0.));
#12521=DIRECTION('center_axis',(0.866025403784439,0.,-0.5));
#12522=DIRECTION('ref_axis',(0.5,0.,0.866025403784439));
#12523=DIRECTION('',(-0.5,0.,-0.866025403784439));
#12524=DIRECTION('',(0.,-1.,0.));
#12525=DIRECTION('',(0.5,0.,0.866025403784439));
#12526=DIRECTION('',(0.,-1.,0.));
#12527=DIRECTION('center_axis',(1.20185167898973E-16,0.,-1.));
#12528=DIRECTION('ref_axis',(1.,0.,1.20185167898973E-16));
#12529=DIRECTION('',(-1.,0.,-1.20185167898973E-16));
#12530=DIRECTION('',(0.,-1.,0.));
#12531=DIRECTION('',(1.,0.,1.20185167898973E-16));
#12532=DIRECTION('center_axis',(-0.866025403784439,0.,-0.5));
#12533=DIRECTION('ref_axis',(0.5,0.,-0.866025403784439));
#12534=DIRECTION('',(-0.5,0.,0.866025403784439));
#12535=DIRECTION('',(0.,-1.,0.));
#12536=DIRECTION('',(0.5,0.,-0.866025403784439));
#12537=DIRECTION('center_axis',(-0.866025403784439,0.,0.5));
#12538=DIRECTION('ref_axis',(-0.5,0.,-0.866025403784439));
#12539=DIRECTION('',(0.5,0.,0.866025403784439));
#12540=DIRECTION('',(0.,-1.,0.));
#12541=DIRECTION('',(-0.5,0.,-0.866025403784439));
#12542=DIRECTION('center_axis',(-2.40370335797945E-16,0.,1.));
#12543=DIRECTION('ref_axis',(-1.,0.,-2.40370335797945E-16));
#12544=DIRECTION('',(1.,0.,2.40370335797945E-16));
#12545=DIRECTION('',(0.,-1.,0.));
#12546=DIRECTION('',(-1.,0.,-2.40370335797945E-16));
#12547=DIRECTION('center_axis',(0.866025403784439,0.,0.5));
#12548=DIRECTION('ref_axis',(-0.5,0.,0.866025403784439));
#12549=DIRECTION('',(0.5,0.,-0.866025403784439));
#12550=DIRECTION('',(-0.5,0.,0.866025403784439));
#12551=DIRECTION('center_axis',(0.,1.,0.));
#12552=DIRECTION('ref_axis',(1.,0.,0.));
#12553=DIRECTION('center_axis',(0.,-1.,0.));
#12554=DIRECTION('ref_axis',(0.,0.,-1.));
#12555=DIRECTION('center_axis',(0.,1.,0.));
#12556=DIRECTION('ref_axis',(1.,0.,0.));
#12557=DIRECTION('center_axis',(0.,1.,0.));
#12558=DIRECTION('ref_axis',(1.,0.,0.));
#12559=DIRECTION('center_axis',(0.,1.,0.));
#12560=DIRECTION('ref_axis',(1.,0.,0.));
#12561=DIRECTION('center_axis',(0.,1.,0.));
#12562=DIRECTION('ref_axis',(1.,0.,0.));
#12563=DIRECTION('',(0.,-1.,0.));
#12564=DIRECTION('center_axis',(0.,1.,0.));
#12565=DIRECTION('ref_axis',(1.,0.,0.));
#12566=DIRECTION('center_axis',(0.,1.,0.));
#12567=DIRECTION('ref_axis',(1.,0.,0.));
#12568=DIRECTION('center_axis',(0.,1.,0.));
#12569=DIRECTION('ref_axis',(0.,0.,1.));
#12570=DIRECTION('center_axis',(0.,-1.,0.));
#12571=DIRECTION('ref_axis',(1.,0.,0.));
#12572=DIRECTION('center_axis',(0.,-1.,0.));
#12573=DIRECTION('ref_axis',(1.,0.,0.));
#12574=DIRECTION('center_axis',(0.,-1.,0.));
#12575=DIRECTION('ref_axis',(1.,0.,0.));
#12576=DIRECTION('',(0.707106781186548,0.707106781186547,8.65956056235493E-17));
#12577=DIRECTION('center_axis',(0.,-1.,0.));
#12578=DIRECTION('ref_axis',(1.,0.,0.));
#12579=DIRECTION('center_axis',(0.,-1.,0.));
#12580=DIRECTION('ref_axis',(1.,0.,0.));
#12581=DIRECTION('',(0.,1.,0.));
#12582=DIRECTION('center_axis',(0.,1.,0.));
#12583=DIRECTION('ref_axis',(1.,0.,0.));
#12584=DIRECTION('center_axis',(0.,-1.,0.));
#12585=DIRECTION('ref_axis',(1.,0.,0.));
#12586=DIRECTION('',(-0.707106781186547,0.707106781186548,-8.65956056235493E-17));
#12587=DIRECTION('center_axis',(0.,-1.,0.));
#12588=DIRECTION('ref_axis',(0.,0.,-1.));
#12589=DIRECTION('center_axis',(0.,-1.,0.));
#12590=DIRECTION('ref_axis',(1.,0.,0.));
#12591=DIRECTION('center_axis',(0.,1.,0.));
#12592=DIRECTION('ref_axis',(1.,0.,0.));
#12593=DIRECTION('center_axis',(0.,1.,0.));
#12594=DIRECTION('ref_axis',(1.,0.,0.));
#12595=DIRECTION('',(-0.447213595499958,0.894427190999916,-5.47678698264203E-17));
#12596=DIRECTION('center_axis',(0.,-1.,0.));
#12597=DIRECTION('ref_axis',(1.,0.,0.));
#12598=DIRECTION('',(0.,1.,0.));
#15594=CARTESIAN_POINT('',(0.,0.,0.));
#15595=CARTESIAN_POINT('Origin',(0.115470053837925,-0.5,-0.2));
#15596=CARTESIAN_POINT('',(0.23094010767585,-0.5,0.));
#15597=CARTESIAN_POINT('',(0.115470053837925,-0.5,-0.2));
#15598=CARTESIAN_POINT('',(0.23094010767585,-0.5,0.));
#15599=CARTESIAN_POINT('',(0.115470053837925,-0.8,-0.2));
#15600=CARTESIAN_POINT('',(0.115470053837925,-0.5,-0.2));
#15601=CARTESIAN_POINT('',(0.23094010767585,-0.8,0.));
#15602=CARTESIAN_POINT('',(0.23094010767585,-0.8,0.));
#15603=CARTESIAN_POINT('',(0.23094010767585,-0.5,0.));
#15604=CARTESIAN_POINT('Origin',(-0.115470053837925,-0.5,-0.2));
#15605=CARTESIAN_POINT('',(-0.115470053837925,-0.5,-0.2));
#15606=CARTESIAN_POINT('',(0.115470053837925,-0.5,-0.2));
#15607=CARTESIAN_POINT('',(-0.115470053837925,-0.8,-0.2));
#15608=CARTESIAN_POINT('',(-0.115470053837925,-0.5,-0.2));
#15609=CARTESIAN_POINT('',(0.115470053837925,-0.8,-0.2));
#15610=CARTESIAN_POINT('Origin',(-0.23094010767585,-0.5,-2.77555756156289E-17));
#15611=CARTESIAN_POINT('',(-0.23094010767585,-0.5,-2.82820063659975E-17));
#15612=CARTESIAN_POINT('',(-0.115470053837925,-0.5,-0.2));
#15613=CARTESIAN_POINT('',(-0.23094010767585,-0.8,-2.77555756156289E-17));
#15614=CARTESIAN_POINT('',(-0.23094010767585,-0.5,-2.82820063659975E-17));
#15615=CARTESIAN_POINT('',(-0.115470053837925,-0.8,-0.2));
#15616=CARTESIAN_POINT('Origin',(-0.115470053837925,-0.5,0.2));
#15617=CARTESIAN_POINT('',(-0.115470053837925,-0.5,0.2));
#15618=CARTESIAN_POINT('',(-0.23094010767585,-0.5,-2.82820063659975E-17));
#15619=CARTESIAN_POINT('',(-0.115470053837925,-0.8,0.2));
#15620=CARTESIAN_POINT('',(-0.115470053837925,-0.5,0.2));
#15621=CARTESIAN_POINT('',(-0.23094010767585,-0.8,-2.82820063659975E-17));
#15622=CARTESIAN_POINT('Origin',(0.115470053837925,-0.5,0.2));
#15623=CARTESIAN_POINT('',(0.115470053837925,-0.5,0.2));
#15624=CARTESIAN_POINT('',(-0.115470053837925,-0.5,0.2));
#15625=CARTESIAN_POINT('',(0.115470053837925,-0.8,0.2));
#15626=CARTESIAN_POINT('',(0.115470053837925,-0.5,0.2));
#15627=CARTESIAN_POINT('',(-0.115470053837925,-0.8,0.2));
#15628=CARTESIAN_POINT('Origin',(0.23094010767585,-0.5,0.));
#15629=CARTESIAN_POINT('',(0.115470053837925,-0.5,0.2));
#15630=CARTESIAN_POINT('',(0.115470053837925,-0.8,0.2));
#15631=CARTESIAN_POINT('Origin',(0.,-0.5,0.));
#15632=CARTESIAN_POINT('Origin',(0.,-0.8,0.));
#15633=CARTESIAN_POINT('Origin',(0.,-1.9,0.));
#15634=CARTESIAN_POINT('',(-0.25,-1.9,3.06161699786838E-17));
#15635=CARTESIAN_POINT('Origin',(0.,-1.9,0.));
#15636=CARTESIAN_POINT('',(-0.24505,-1.9,3.00099698131059E-17));
#15637=CARTESIAN_POINT('Origin',(0.,-1.9,0.));
#15638=CARTESIAN_POINT('Origin',(0.,-3.,0.));
#15639=CARTESIAN_POINT('',(-0.25,-3.,3.06161699786838E-17));
#15640=CARTESIAN_POINT('',(-0.25,-3.,3.06161699786838E-17));
#15641=CARTESIAN_POINT('Origin',(0.,-3.,0.));
#15642=CARTESIAN_POINT('Origin',(0.,-3.,0.));
#15643=CARTESIAN_POINT('Origin',(0.375,0.5,0.));
#15644=CARTESIAN_POINT('',(-0.375,0.5,-4.59242549680257E-17));
#15645=CARTESIAN_POINT('Origin',(0.,0.5,0.));
#15646=CARTESIAN_POINT('Origin',(0.,0.475,0.));
#15647=CARTESIAN_POINT('',(-0.425,0.45,-5.20474889637625E-17));
#15648=CARTESIAN_POINT('Origin',(0.,0.45,0.));
#15649=CARTESIAN_POINT('',(-0.4,0.475,-4.89858719658941E-17));
#15650=CARTESIAN_POINT('Origin',(0.,0.24,0.));
#15651=CARTESIAN_POINT('',(-0.425,0.0299999999999998,-5.20474889637625E-17));
#15652=CARTESIAN_POINT('Origin',(0.,0.0299999999999998,0.));
#15653=CARTESIAN_POINT('',(-0.425,0.24,-5.20474889637625E-17));
#15654=CARTESIAN_POINT('Origin',(0.,0.0150000000000001,0.));
#15655=CARTESIAN_POINT('',(-0.395,4.85722573273506E-17,-4.83735485663204E-17));
#15656=CARTESIAN_POINT('Origin',(0.,0.,0.));
#15657=CARTESIAN_POINT('',(-0.41,0.0150000000000001,-5.02105187650415E-17));
#15658=CARTESIAN_POINT('Origin',(0.27,0.,0.));
#15659=CARTESIAN_POINT('',(-0.27,0.,-3.30654635769785E-17));
#15660=CARTESIAN_POINT('Origin',(0.,0.,0.));
#15661=CARTESIAN_POINT('Origin',(0.,-0.02,0.));
#15662=CARTESIAN_POINT('',(-0.24505,-0.0498999999999999,3.00099698131059E-17));
#15663=CARTESIAN_POINT('Origin',(0.,-0.0498999999999999,0.));
#15664=CARTESIAN_POINT('',(-0.26,-0.02,-3.18408167778312E-17));
#15665=CARTESIAN_POINT('Origin',(0.,-0.995,0.));
#15666=CARTESIAN_POINT('',(-0.24505,-0.995,-3.00099698131059E-17));
#18925=UNCERTAINTY_MEASURE_WITH_UNIT(LENGTH_MEASURE(0.001),#19044,
'DISTANCE_ACCURACY_VALUE',
'Maximum model space distance between geometric entities at asserted c
onnectivities');
#18972=UNCERTAINTY_MEASURE_WITH_UNIT(LENGTH_MEASURE(0.001),#19044,
'DISTANCE_ACCURACY_VALUE',
'Maximum model space distance between geometric entities at asserted c
onnectivities');
#18996=(
GEOMETRIC_REPRESENTATION_CONTEXT(3)
GLOBAL_UNCERTAINTY_ASSIGNED_CONTEXT((#18925))
GLOBAL_UNIT_ASSIGNED_CONTEXT((#19044,#19046,#19047))
REPRESENTATION_CONTEXT('','3D')
);
#19043=(
GEOMETRIC_REPRESENTATION_CONTEXT(3)
GLOBAL_UNCERTAINTY_ASSIGNED_CONTEXT((#18972))
GLOBAL_UNIT_ASSIGNED_CONTEXT((#19044,#19046,#19047))
REPRESENTATION_CONTEXT('','3D')
);
#19044=(
LENGTH_UNIT()
NAMED_UNIT(*)
SI_UNIT(.CENTI.,.METRE.)
);
#19046=(
NAMED_UNIT(*)
PLANE_ANGLE_UNIT()
SI_UNIT($,.RADIAN.)
);
#19047=(
NAMED_UNIT(*)
SI_UNIT($,.STERADIAN.)
SOLID_ANGLE_UNIT()
);
#19071=SHAPE_DEFINITION_REPRESENTATION(#19141,#19329);
#19141=PRODUCT_DEFINITION_SHAPE('',$,#19400);
#19329=SHAPE_REPRESENTATION('',(#10640),#18996);
#19376=PRODUCT_DEFINITION_CONTEXT('part definition',#19588,'design');
#19400=PRODUCT_DEFINITION('2026-11-03-00-38-46-496','M5x30 frame screw',
#19470,#19376);
#19470=PRODUCT_DEFINITION_FORMATION('',$,#19613);
#19588=APPLICATION_CONTEXT(
'Core Data for Automotive Mechanical Design Process');
#19589=PRODUCT_CONTEXT('part definition',#19588,'mechanical');
#19613=PRODUCT('2026-11-03-00-38-46-496','M5x30 frame screw',
'M5x30 frame screw',(#19589));
#19663=PRESENTATION_STYLE_ASSIGNMENT((#19669));
#19669=SURFACE_STYLE_USAGE(.BOTH.,#19675);
#19675=SURFACE_SIDE_STYLE('',(#19681));
#19681=SURFACE_STYLE_FILL_AREA(#19687);
#19687=FILL_AREA_STYLE('CAD Library Painted - Graphite',(#19693));
#19693=FILL_AREA_STYLE_COLOUR('CAD Library Painted - Graphite',#19699);
#19699=COLOUR_RGB('CAD Library Painted - Graphite',0.168627450980392,0.192156862745098,
0.231372549019608);
ENDSEC;
END-ISO-10303-21;
